ISO-10303-21;
HEADER;
/* Generated by software containing ST-Developer
 * from STEP Tools, Inc. (www.steptools.com) 
 */

FILE_DESCRIPTION(
/* description */ (''),
/* implementation_level */ '2;1');

FILE_NAME(
/* name */ 'Nut.step',
/* time_stamp */ '2026-10-05T01:33:24-07:00',
/* author */ (''),
/* organization */ (''),
/* preprocessor_version */ 'ST-DEVELOPER v20.2',
/* originating_system */ 'Autodesk Translation Framework v15.15.0.0',
/* authorisation */ '');

FILE_SCHEMA (('AUTOMOTIVE_DESIGN { 1 0 10303 214 3 1 1 }'));
ENDSEC;

DATA;
#10=MECHANICAL_DESIGN_GEOMETRIC_PRESENTATION_REPRESENTATION('',(#88),#1128);
#58=CONICAL_SURFACE('',#695,5.75,0.785398163397451);
#59=CONICAL_SURFACE('',#700,5.75,0.785398163397451);
#68=SHAPE_REPRESENTATION_RELATIONSHIP('SRR','None',#1172,#78);
#78=ADVANCED_BREP_SHAPE_REPRESENTATION('',(#98),#1124);
#88=STYLED_ITEM('',(#1227),#98);
#98=MANIFOLD_SOLID_BREP('Body1',#527);
#111=LINE('',#1040,#128);
#112=LINE('',#1045,#129);
#113=LINE('',#1048,#130);
#128=VECTOR('',#860,5.75);
#129=VECTOR('',#867,6.);
#130=VECTOR('',#870,5.75);
#142=CYLINDRICAL_SURFACE('',#698,6.);
#170=FACE_OUTER_BOUND('',#211,.T.);
#171=FACE_OUTER_BOUND('',#212,.T.);
#172=FACE_OUTER_BOUND('',#213,.T.);
#173=FACE_OUTER_BOUND('',#214,.T.);
#174=FACE_OUTER_BOUND('',#215,.T.);
#211=EDGE_LOOP('',(#412,#413,#414,#415));
#212=EDGE_LOOP('',(#416,#417,#418,#419));
#213=EDGE_LOOP('',(#420,#421,#422,#423));
#214=EDGE_LOOP('',(#424));
#215=EDGE_LOOP('',(#425));
#249=CIRCLE('',#696,6.);
#250=CIRCLE('',#697,5.5);
#251=CIRCLE('',#699,6.);
#252=CIRCLE('',#701,5.5);
#283=VERTEX_POINT('',#1037);
#284=VERTEX_POINT('',#1039);
#285=VERTEX_POINT('',#1043);
#286=VERTEX_POINT('',#1047);
#328=EDGE_CURVE('',#283,#283,#249,.T.);
#329=EDGE_CURVE('',#283,#284,#111,.T.);
#330=EDGE_CURVE('',#284,#284,#250,.T.);
#331=EDGE_CURVE('',#285,#285,#251,.T.);
#332=EDGE_CURVE('',#285,#283,#112,.T.);
#333=EDGE_CURVE('',#285,#286,#113,.T.);
#334=EDGE_CURVE('',#286,#286,#252,.T.);
#412=ORIENTED_EDGE('',*,*,#328,.F.);
#413=ORIENTED_EDGE('',*,*,#329,.T.);
#414=ORIENTED_EDGE('',*,*,#330,.T.);
#415=ORIENTED_EDGE('',*,*,#329,.F.);
#416=ORIENTED_EDGE('',*,*,#331,.F.);
#417=ORIENTED_EDGE('',*,*,#332,.T.);
#418=ORIENTED_EDGE('',*,*,#328,.T.);
#419=ORIENTED_EDGE('',*,*,#332,.F.);
#420=ORIENTED_EDGE('',*,*,#331,.T.);
#421=ORIENTED_EDGE('',*,*,#333,.T.);
#422=ORIENTED_EDGE('',*,*,#334,.F.);
#423=ORIENTED_EDGE('',*,*,#333,.F.);
#424=ORIENTED_EDGE('',*,*,#334,.T.);
#425=ORIENTED_EDGE('',*,*,#330,.F.);
#472=PLANE('',#702);
#473=PLANE('',#703);
#504=ADVANCED_FACE('',(#170),#58,.T.);
#505=ADVANCED_FACE('',(#171),#142,.T.);
#506=ADVANCED_FACE('',(#172),#59,.T.);
#507=ADVANCED_FACE('',(#173),#472,.T.);
#508=ADVANCED_FACE('',(#174),#473,.T.);
#527=CLOSED_SHELL('',(#504,#505,#506,#507,#508));
#694=AXIS2_PLACEMENT_3D('',#1035,#854,#855);
#695=AXIS2_PLACEMENT_3D('',#1036,#856,#857);
#696=AXIS2_PLACEMENT_3D('',#1038,#858,#859);
#697=AXIS2_PLACEMENT_3D('',#1041,#861,#862);
#698=AXIS2_PLACEMENT_3D('',#1042,#863,#864);
#699=AXIS2_PLACEMENT_3D('',#1044,#865,#866);
#700=AXIS2_PLACEMENT_3D('',#1046,#868,#869);
#701=AXIS2_PLACEMENT_3D('',#1049,#871,#872);
#702=AXIS2_PLACEMENT_3D('',#1050,#873,#874);
#703=AXIS2_PLACEMENT_3D('',#1051,#875,#876);
#854=DIRECTION('axis',(0.,0.,1.));
#855=DIRECTION('refdir',(1.,0.,0.));
#856=DIRECTION('center_axis',(1.,0.,0.));
#857=DIRECTION('ref_axis',(0.,0.,-1.));
#858=DIRECTION('center_axis',(1.,0.,0.));
#859=DIRECTION('ref_axis',(0.,0.,-1.));
#860=DIRECTION('',(-0.707106781186546,8.65956056235496E-17,-0.707106781186549));
#861=DIRECTION('center_axis',(1.,0.,0.));
#862=DIRECTION('ref_axis',(0.,0.,-1.));
#863=DIRECTION('center_axis',(1.,0.,0.));
#864=DIRECTION('ref_axis',(0.,0.,-1.));
#865=DIRECTION('center_axis',(1.,0.,0.));
#866=DIRECTION('ref_axis',(0.,0.,-1.));
#867=DIRECTION('',(-1.,0.,0.));
#868=DIRECTION('center_axis',(-1.,0.,0.));
#869=DIRECTION('ref_axis',(0.,0.,-1.));
#870=DIRECTION('',(0.707106781186546,-8.65956056235496E-17,-0.707106781186549));
#871=DIRECTION('center_axis',(1.,0.,0.));
#872=DIRECTION('ref_axis',(0.,0.,-1.));
#873=DIRECTION('center_axis',(1.,0.,0.));
#874=DIRECTION('ref_axis',(0.,0.,-1.));
#875=DIRECTION('center_axis',(-1.,0.,0.));
#876=DIRECTION('ref_axis',(0.,0.,1.));
#1035=CARTESIAN_POINT('',(0.,0.,0.));
#1036=CARTESIAN_POINT('Origin',(20.4854431734887,0.,0.));
#1037=CARTESIAN_POINT('',(20.7354431734887,-7.34788079488412E-16,6.));
#1038=CARTESIAN_POINT('Origin',(20.7354431734887,0.,0.));
#1039=CARTESIAN_POINT('',(20.2354431734887,-6.73555739531044E-16,5.5));
#1040=CARTESIAN_POINT('',(20.4854431734887,-7.04171909509728E-16,5.75));
#1041=CARTESIAN_POINT('Origin',(20.2354431734887,0.,0.));
#1042=CARTESIAN_POINT('Origin',(21.7354431734887,0.,0.));
#1043=CARTESIAN_POINT('',(22.7354431734887,-7.34788079488412E-16,6.));
#1044=CARTESIAN_POINT('Origin',(22.7354431734887,0.,0.));
#1045=CARTESIAN_POINT('',(21.7354431734887,-7.34788079488412E-16,6.));
#1046=CARTESIAN_POINT('Origin',(22.9854431734887,0.,0.));
#1047=CARTESIAN_POINT('',(23.2354431734887,-6.73555739531044E-16,5.5));
#1048=CARTESIAN_POINT('',(22.9854431734887,7.04171909509728E-16,5.75));
#1049=CARTESIAN_POINT('Origin',(23.2354431734887,0.,0.));
#1050=CARTESIAN_POINT('Origin',(23.2354431734887,0.,0.));
#1051=CARTESIAN_POINT('Origin',(20.2354431734887,0.,-5.5));
#1112=UNCERTAINTY_MEASURE_WITH_UNIT(LENGTH_MEASURE(0.01),#1129,
'DISTANCE_ACCURACY_VALUE',
'Maximum model space distance between geometric entities at asserted c
onnectivities');
#1116=UNCERTAINTY_MEASURE_WITH_UNIT(LENGTH_MEASURE(0.01),#1129,
'DISTANCE_ACCURACY_VALUE',
'Maximum model space distance between geometric entities at asserted c
onnectivities');
#1124=(
GEOMETRIC_REPRESENTATION_CONTEXT(3)
GLOBAL_UNCERTAINTY_ASSIGNED_CONTEXT((#1112))
GLOBAL_UNIT_ASSIGNED_CONTEXT((#1129,#1131,#1132))
REPRESENTATION_CONTEXT('','3D')
);
#1128=(
GEOMETRIC_REPRESENTATION_CONTEXT(3)
GLOBAL_UNCERTAINTY_ASSIGNED_CONTEXT((#1116))
GLOBAL_UNIT_ASSIGNED_CONTEXT((#1129,#1131,#1132))
REPRESENTATION_CONTEXT('','3D')
);
#1129=(
LENGTH_UNIT()
NAMED_UNIT(*)
SI_UNIT(.MILLI.,.METRE.)
);
#1131=(
NAMED_UNIT(*)
PLANE_ANGLE_UNIT()
SI_UNIT($,.RADIAN.)
);
#1132=(
NAMED_UNIT(*)
SI_UNIT($,.STERADIAN.)
SOLID_ANGLE_UNIT()
);
#1140=SHAPE_DEFINITION_REPRESENTATION(#1151,#1172);
#1151=PRODUCT_DEFINITION_SHAPE('',$,#1184);
#1172=SHAPE_REPRESENTATION('',(#694),#1124);
#1176=PRODUCT_DEFINITION_CONTEXT('part definition',#1211,'design');
#1184=PRODUCT_DEFINITION('Nut','Nut',#1195,#1176);
#1195=PRODUCT_DEFINITION_FORMATION('',$,#1220);
#1211=APPLICATION_CONTEXT(
'Core Data for Automotive Mechanical Design Process');
#1212=PRODUCT_CONTEXT('part definition',#1211,'mechanical');
#1220=PRODUCT('Nut','Nut',$,(#1212));
#1227=PRESENTATION_STYLE_ASSIGNMENT((#1231));
#1231=SURFACE_STYLE_USAGE(.BOTH.,#1235);
#1235=SURFACE_SIDE_STYLE('',(#1239));
#1239=SURFACE_STYLE_FILL_AREA(#1243);
#1243=FILL_AREA_STYLE('Opaque(77,77,77)',(#1247));
#1247=FILL_AREA_STYLE_COLOUR('Opaque(77,77,77)',#1251);
#1251=COLOUR_RGB('Opaque(77,77,77)', 0.72549020, 0.75294118, 0.79215686);
ENDSEC;
END-ISO-10303-21;
